ISO-10303-21;
HEADER;
FILE_DESCRIPTION (('STEP AP214'),
    '1' );
FILE_NAME ('Slide Locking Screw.step',
    '2026-10-09T18:50:44',
    ( '' ),
    ( '' ),
    'SwSTEP 2.0',
    'SolidWorks 2026',
    '' );
FILE_SCHEMA (( 'AUTOMOTIVE_DESIGN' ));
ENDSEC;

DATA;
#1=DIRECTION ( 'NONE',  ( 1.000000000000000000, 1.000000000000000078E-15, 0.000000000000000000 ) ) ;
#10=FACE_OUTER_BOUND ( 'NONE', #5268, .T. ) ;
#21=CYLINDRICAL_SURFACE ( 'NONE', #12948, 3.000000000000002665 ) ;
#86=CARTESIAN_POINT ( 'NONE',  ( -3.508527451664998686, -47.80641709811465745, -6.247689735156000346 ) ) ;
#114=CARTESIAN_POINT ( 'NONE',  ( -9.989347722329675605, -44.50737899243799944, -5.497689735156000346 ) ) ;
#121=CARTESIAN_POINT ( 'NONE',  ( -1.821162622431182765, -43.50737899243799234, -5.497689735156000346 ) ) ;
#134=CARTESIAN_POINT ( 'NONE',  ( -3.508527451664998686, -47.37340439622244048, -6.997689735156000346 ) ) ;
#145=DIRECTION ( 'NONE',  ( 8.660254037844386422E-16, -0.8660254037844387076, -0.4999999999999998890 ) ) ;
#152=CARTESIAN_POINT ( 'NONE',  ( -1.821162622431182765, -43.50737899243799234, -5.497689735156000346 ) ) ;
#266=EDGE_CURVE ( 'NONE', #5839, #14925, #4584, .T. ) ;
#290=PLANE ( 'NONE',  #9367 ) ;
#305=DIRECTION ( 'NONE',  ( -8.673617379884027583E-16, 1.000000000000000000, 0.000000000000000000 ) ) ;
#311=ORIENTED_EDGE ( 'NONE', *, *, #9034, .F. ) ;
#350=FILL_AREA_STYLE ('',( #10818 ) ) ;
#374=VERTEX_POINT ( 'NONE', #1959 ) ;
#415=VERTEX_POINT ( 'NONE', #9058 ) ;
#431=ORIENTED_EDGE ( 'NONE', *, *, #15117, .F. ) ;
#438=AXIS2_PLACEMENT_3D ( 'NONE', #1903, #3121, #4272 ) ;
#442=ORIENTED_EDGE ( 'NONE', *, *, #8119, .T. ) ;
#525=DIRECTION ( 'NONE',  ( -5.000000000000000389E-16, 0.4999999999999998890, 0.8660254037844387076 ) ) ;
#565=AXIS2_PLACEMENT_3D ( 'NONE', #1376, #13021, #11699 ) ;
#574=ORIENTED_EDGE ( 'NONE', *, *, #9034, .T. ) ;
#590=EDGE_CURVE ( 'NONE', #5768, #8983, #12195, .T. ) ;
#605=ORIENTED_EDGE ( 'NONE', *, *, #6254, .F. ) ;
#606=DIRECTION ( 'NONE',  ( -1.011922027653136551E-15, 1.000000000000000000, 0.000000000000000000 ) ) ;
#622=DIRECTION ( 'NONE',  ( -1.000000000000000078E-15, 1.000000000000000000, 0.000000000000000000 ) ) ;
#627=CARTESIAN_POINT ( 'NONE',  ( -1.508527451665001351, -45.27812899243799194, -5.497689735156000346 ) ) ;
#670=AXIS2_PLACEMENT_3D ( 'NONE', #8463, #2659, #7310 ) ;
#741=STYLED_ITEM ( 'NONE', ( #11809 ), #7566 ) ;
#756=DIRECTION ( 'NONE',  ( 1.000000000000000000, 1.000000000000000078E-15, 0.000000000000000000 ) ) ;
#771=DIRECTION ( 'NONE',  ( -8.673617379884027583E-16, 1.000000000000000000, 0.000000000000000000 ) ) ;
#786=LINE ( 'NONE', #6578, #10259 ) ;
#793=PRODUCT_DEFINITION_SHAPE ( 'NONE', 'NONE',  #7495 ) ;
#824=LINE ( 'NONE', #134, #11341 ) ;
#879=DIRECTION ( 'NONE',  ( -8.673617379884027583E-16, 1.000000000000000000, 0.000000000000000000 ) ) ;
#890=DIRECTION ( 'NONE',  ( -1.000000000000000000, -1.000000000000000078E-15, 0.000000000000000000 ) ) ;
#912=ORIENTED_EDGE ( 'NONE', *, *, #1524, .T. ) ;
#1012=DIRECTION ( 'NONE',  ( 1.000000000000000000, 1.000000000000000078E-15, 0.000000000000000000 ) ) ;
#1078=ORIENTED_EDGE ( 'NONE', *, *, #8722, .T. ) ;
#1093=CARTESIAN_POINT ( 'NONE',  ( -1.508527451665001351, -44.77532818486911736, -5.497689735156003010 ) ) ;
#1111=ORIENTED_EDGE ( 'NONE', *, *, #8455, .F. ) ;
#1143=VERTEX_POINT ( 'NONE', #11973 ) ;
#1154=DIRECTION ( 'NONE',  ( -1.156482317317870344E-15, 1.000000000000000000, 0.000000000000000000 ) ) ;
#1205=LINE ( 'NONE', #4730, #9219 ) ;
#1284=ORIENTED_EDGE ( 'NONE', *, *, #14044, .T. ) ;
#1314=EDGE_CURVE ( 'NONE', #11680, #6476, #3622, .T. ) ;
#1376=CARTESIAN_POINT ( 'NONE',  ( -3.508527451665000463, -45.20834088676133433, -6.247689735156000346 ) ) ;
#1406=AXIS2_PLACEMENT_3D ( 'NONE', #13534, #8929, #5266 ) ;
#1474=COLOUR_RGB ( '', 0.09019608, 0.27058824, 0.51372549) ;
#1485=SURFACE_SIDE_STYLE ('',( #12972 ) ) ;
#1524=EDGE_CURVE ( 'NONE', #11896, #6476, #14383, .T. ) ;
#1526=AXIS2_PLACEMENT_3D ( 'NONE', #7238, #8475, #305 ) ;
#1616=CYLINDRICAL_SURFACE ( 'NONE', #9730, 2.000000000000001776 ) ;
#1618=DIRECTION ( 'NONE',  ( 1.011922027653136551E-15, -1.000000000000000000, 0.000000000000000000 ) ) ;
#1650=EDGE_CURVE ( 'NONE', #374, #13801, #1205, .T. ) ;
#1659=ORIENTED_EDGE ( 'NONE', *, *, #14390, .F. ) ;
#1673=PLANE ( 'NONE',  #438 ) ;
#1686=ADVANCED_FACE ( 'NONE', ( #10613 ), #12691, .T. ) ;
#1689=DIRECTION ( 'NONE',  ( 1.000000000000000000, 1.000000000000000078E-15, 0.000000000000000000 ) ) ;
#1710=CARTESIAN_POINT ( 'NONE',  ( -1.821162622431176770, -49.50737899243799944, -5.497689735156000346 ) ) ;
#1750=VERTEX_POINT ( 'NONE', #10308 ) ;
#1761=VECTOR ( 'NONE', #9432, 1000.000000000000000 ) ;
#1768=ORIENTED_EDGE ( 'NONE', *, *, #8455, .T. ) ;
#1771=ORIENTED_EDGE ( 'NONE', *, *, #1860, .F. ) ;
#1860=EDGE_CURVE ( 'NONE', #6476, #14925, #2660, .T. ) ;
#1903=CARTESIAN_POINT ( 'NONE',  ( -3.508527451664999575, -46.50737899243799234, -5.497689735156000346 ) ) ;
#1923=ORIENTED_EDGE ( 'NONE', *, *, #3003, .T. ) ;
#1959=CARTESIAN_POINT ( 'NONE',  ( -3.508527451665000463, -45.64135358865355840, -3.997689735156000790 ) ) ;
#1973=ADVANCED_FACE ( 'NONE', ( #12514 ), #2035, .T. ) ;
#2023=CARTESIAN_POINT ( 'NONE',  ( -7.758527451664999575, -46.50737899243799944, -5.497689735156000346 ) ) ;
#2035=PLANE ( 'NONE',  #8386 ) ;
#2074=DIRECTION ( 'NONE',  ( 1.000000000000000000, 1.000000000000000078E-15, 0.000000000000000000 ) ) ;
#2082=FACE_OUTER_BOUND ( 'NONE', #10563, .T. ) ;
#2089=( NAMED_UNIT ( * ) PLANE_ANGLE_UNIT ( ) SI_UNIT ( $, .RADIAN. ) );
#2116=DIRECTION ( 'NONE',  ( -1.000000000000000000, -1.000000000000000078E-15, 0.000000000000000000 ) ) ;
#2120=EDGE_CURVE ( 'NONE', #14475, #11896, #13290, .T. ) ;
#2166=CYLINDRICAL_SURFACE ( 'NONE', #10265, 2.000000000000001776 ) ;
#2190=VECTOR ( 'NONE', #12683, 1000.000000000000000 ) ;
#2214=CARTESIAN_POINT ( 'NONE',  ( -1.508527451664999575, -46.50737899243799234, -3.997689735156000790 ) ) ;
#2217=DIRECTION ( 'NONE',  ( 1.000000000000000000, 1.000000000000000078E-15, 0.000000000000000000 ) ) ;
#2228=ORIENTED_EDGE ( 'NONE', *, *, #14180, .F. ) ;
#2240=ORIENTED_EDGE ( 'NONE', *, *, #8119, .F. ) ;
#2276=CARTESIAN_POINT ( 'NONE',  ( -7.758527451664997798, -48.50737899243800655, -5.497689735156000346 ) ) ;
#2289=CARTESIAN_POINT ( 'NONE',  ( -3.508527451664997798, -48.23942980000687442, -5.497689735155999458 ) ) ;
#2422=VERTEX_POINT ( 'NONE', #1093 ) ;
#2433=DIRECTION ( 'NONE',  ( 1.000000000000000000, 1.000000000000000078E-15, 0.000000000000000000 ) ) ;
#2441=EDGE_LOOP ( 'NONE', ( #7965, #7075, #10384, #1771 ) ) ;
#2462=ORIENTED_EDGE ( 'NONE', *, *, #12248, .T. ) ;
#2471=VERTEX_POINT ( 'NONE', #6960 ) ;
#2492=AXIS2_PLACEMENT_3D ( 'NONE', #13672, #2116, #7830 ) ;
#2498=DIRECTION ( 'NONE',  ( -1.000000000000000000, -1.000000000000000078E-15, 0.000000000000000000 ) ) ;
#2659=DIRECTION ( 'NONE',  ( 1.000000000000000000, 1.000000000000000078E-15, 0.000000000000000000 ) ) ;
#2660=LINE ( 'NONE', #13151, #14869 ) ;
#2673=CARTESIAN_POINT ( 'NONE',  ( -3.508527451664998686, -47.80641709811465745, -4.747689735156000346 ) ) ;
#2687=ORIENTED_EDGE ( 'NONE', *, *, #15117, .T. ) ;
#2689=DIRECTION ( 'NONE',  ( 0.7071067811865487940, -0.7071067811865463515, 8.659560562354927928E-17 ) ) ;
#2721=ADVANCED_FACE ( 'NONE', ( #3869 ), #10433, .T. ) ;
#2762=AXIS2_PLACEMENT_3D ( 'NONE', #2023, #6672, #879 ) ;
#2763=EDGE_CURVE ( 'NONE', #1143, #374, #7642, .T. ) ;
#2935=APPLICATION_CONTEXT ( 'automotive_design' ) ;
#2999=CARTESIAN_POINT ( 'NONE',  ( -3.508527451664999575, -46.50737899243799234, -6.997689735156000346 ) ) ;
#3003=EDGE_CURVE ( 'NONE', #12315, #1143, #11932, .T. ) ;
#3038=DIRECTION ( 'NONE',  ( 5.000000000000000389E-16, -0.4999999999999998890, -0.8660254037844387076 ) ) ;
#3070=DIRECTION ( 'NONE',  ( -1.000000000000000078E-15, 1.000000000000000000, 0.000000000000000000 ) ) ;
#3078=VECTOR ( 'NONE', #525, 1000.000000000000000 ) ;
#3121=DIRECTION ( 'NONE',  ( 1.000000000000000000, 1.000000000000000078E-15, 0.000000000000000000 ) ) ;
#3127=DIRECTION ( 'NONE',  ( -9.702032863404950344E-16, 1.000000000000000000, 0.000000000000000000 ) ) ;
#3138=CARTESIAN_POINT ( 'NONE',  ( -3.508527451664999575, -46.50737899243799234, -3.997689735156000790 ) ) ;
#3153=ADVANCED_BREP_SHAPE_REPRESENTATION ( '', ( #7566, #6789 ), #8516 ) ;
#3161=DIRECTION ( 'NONE',  ( 1.000000000000000078E-15, -1.000000000000000000, 0.000000000000000000 ) ) ;
#3178=DIRECTION ( 'NONE',  ( 1.000000000000000000, 1.000000000000000078E-15, 0.000000000000000000 ) ) ;
#3231=DIRECTION ( 'NONE',  ( -1.156482317317870344E-15, 1.000000000000000000, 0.000000000000000000 ) ) ;
#3235=AXIS2_PLACEMENT_3D ( 'NONE', #13228, #11223, #5400 ) ;
#3349=CARTESIAN_POINT ( 'NONE',  ( -3.508527451665000463, -45.20834088676133433, -4.747689735156000346 ) ) ;
#3512=DIRECTION ( 'NONE',  ( 1.000000000000000000, 1.000000000000000078E-15, 0.000000000000000000 ) ) ;
#3528=VERTEX_POINT ( 'NONE', #9720 ) ;
#3537=CARTESIAN_POINT ( 'NONE',  ( -3.508527451664999575, -46.50737899243799234, -6.997689735156000346 ) ) ;
#3622=CIRCLE ( 'NONE', #5566, 3.000000000000002665 ) ;
#3650=DIRECTION ( 'NONE',  ( -5.000000000000000389E-16, 0.4999999999999998890, -0.8660254037844387076 ) ) ;
#3664=CARTESIAN_POINT ( 'NONE',  ( -9.989347722329670276, -49.50737899243800655, -5.497689735156000346 ) ) ;
#3735=ORIENTED_EDGE ( 'NONE', *, *, #8990, .T. ) ;
#3758=AXIS2_PLACEMENT_3D ( 'NONE', #4276, #13688, #3127 ) ;
#3789=CARTESIAN_POINT ( 'NONE',  ( -7.758527451664999575, -46.50737899243799944, -5.497689735156000346 ) ) ;
#3835=PRODUCT_CONTEXT ( 'NONE', #5084, 'mechanical' ) ;
#3838=EDGE_CURVE ( 'NONE', #11680, #8983, #13992, .T. ) ;
#3852=SURFACE_STYLE_USAGE ( .BOTH. , #1485 ) ;
#3860=VECTOR ( 'NONE', #3161, 1000.000000000000000 ) ;
#3869=FACE_OUTER_BOUND ( 'NONE', #11652, .T. ) ;
#3883=EDGE_CURVE ( 'NONE', #4490, #415, #10471, .T. ) ;
#3922=ORIENTED_EDGE ( 'NONE', *, *, #13048, .T. ) ;
#3930=LINE ( 'NONE', #9960, #9746 ) ;
#3931=SHAPE_REPRESENTATION ( 'Slide Locking Screw', ( #6789 ), #8516 ) ;
#3974=ORIENTED_EDGE ( 'NONE', *, *, #13552, .T. ) ;
#3995=PLANE ( 'NONE',  #6322 ) ;
#4066=ORIENTED_EDGE ( 'NONE', *, *, #14180, .T. ) ;
#4075=DIRECTION ( 'NONE',  ( 5.000000000000000389E-16, -0.4999999999999998890, -0.8660254037844387076 ) ) ;
#4147=CARTESIAN_POINT ( 'NONE',  ( -7.758527451665001351, -44.50737899243799944, -5.497689735156000346 ) ) ;
#4161=DIRECTION ( 'NONE',  ( -0.4999999999999985012, -0.8660254037844393737, 0.000000000000000000 ) ) ;
#4173=ADVANCED_FACE ( 'NONE', ( #13878 ), #8113, .T. ) ;
#4176=DIRECTION ( 'NONE',  ( -9.702032863404950344E-16, 1.000000000000000000, 0.000000000000000000 ) ) ;
#4227=DIRECTION ( 'NONE',  ( -1.000000000000000078E-15, 1.000000000000000000, 0.000000000000000000 ) ) ;
#4272=DIRECTION ( 'NONE',  ( -1.000000000000000078E-15, 1.000000000000000000, 0.000000000000000000 ) ) ;
#4276=CARTESIAN_POINT ( 'NONE',  ( -1.508527451664999575, -46.50737899243799234, -5.497689735156000346 ) ) ;
#4326=UNCERTAINTY_MEASURE_WITH_UNIT (LENGTH_MEASURE( 1.000000000000000082E-05 ), #4858, 'distance_accuracy_value', 'NONE');
#4332=ORIENTED_EDGE ( 'NONE', *, *, #8990, .F. ) ;
#4336=ORIENTED_EDGE ( 'NONE', *, *, #12759, .T. ) ;
#4381=CARTESIAN_POINT ( 'NONE',  ( 0.000000000000000000, 0.000000000000000000, 0.000000000000000000 ) ) ;
#4490=VERTEX_POINT ( 'NONE', #5224 ) ;
#4554=ORIENTED_EDGE ( 'NONE', *, *, #6254, .T. ) ;
#4584=LINE ( 'NONE', #152, #12416 ) ;
#4593=ADVANCED_FACE ( 'NONE', ( #5517 ), #10179, .T. ) ;
#4600=DIRECTION ( 'NONE',  ( -8.660254037844387408E-16, 0.8660254037844387076, 0.4999999999999998890 ) ) ;
#4604=EDGE_LOOP ( 'NONE', ( #12968, #5174, #9689, #14944 ) ) ;
#4661=ADVANCED_FACE ( 'NONE', ( #8341 ), #21, .T. ) ;
#4673=PRODUCT_DEFINITION_CONTEXT ( 'detailed design', #2935, 'design' ) ;
#4690=LINE ( 'NONE', #3537, #9878 ) ;
#4730=CARTESIAN_POINT ( 'NONE',  ( -3.508527451665000463, -45.20834088676133433, -4.747689735156000346 ) ) ;
#4741=LINE ( 'NONE', #11546, #5483 ) ;
#4761=CONICAL_SURFACE ( 'NONE', #11353, 2.000000000000001776, 0.7853981633974476129 ) ;
#4858=( LENGTH_UNIT ( ) NAMED_UNIT ( * ) SI_UNIT ( .MILLI., .METRE. ) );
#4861=ADVANCED_FACE ( 'NONE', ( #10960, #12257 ), #3995, .F. ) ;
#4877=CLOSED_SHELL ( 'NONE', ( #6731, #7399, #4661, #10269, #8764, #13404, #1686, #11748, #5964, #10005, #1973, #2721, #4593, #4173, #7854, #6060, #4861 ) ) ;
#4905=PLANE ( 'NONE',  #565 ) ;
#4907=PLANE ( 'NONE',  #14218 ) ;
#5084=APPLICATION_CONTEXT ( 'automotive_design' ) ;
#5145=EDGE_CURVE ( 'NONE', #6476, #11680, #5423, .T. ) ;
#5157=EDGE_LOOP ( 'NONE', ( #4066, #442, #13026, #7199 ) ) ;
#5174=ORIENTED_EDGE ( 'NONE', *, *, #266, .T. ) ;
#5224=CARTESIAN_POINT ( 'NONE',  ( -1.508527451664999575, -47.37340439622243338, -3.997689735156000790 ) ) ;
#5245=CARTESIAN_POINT ( 'NONE',  ( -7.758527451664999575, -46.50737899243799944, -5.497689735156000346 ) ) ;
#5252=ORIENTED_EDGE ( 'NONE', *, *, #3883, .F. ) ;
#5266=DIRECTION ( 'NONE',  ( -8.673617379884027583E-16, 1.000000000000000000, 0.000000000000000000 ) ) ;
#5268=EDGE_LOOP ( 'NONE', ( #431, #11313, #6838, #6857 ) ) ;
#5400=DIRECTION ( 'NONE',  ( -8.673617379884027583E-16, 1.000000000000000000, 0.000000000000000000 ) ) ;
#5415=EDGE_CURVE ( 'NONE', #7352, #4490, #13138, .T. ) ;
#5423=CIRCLE ( 'NONE', #3235, 3.000000000000002665 ) ;
#5463=FACE_OUTER_BOUND ( 'NONE', #5157, .T. ) ;
#5483=VECTOR ( 'NONE', #3512, 1000.000000000000000 ) ;
#5517=FACE_OUTER_BOUND ( 'NONE', #8032, .T. ) ;
#5566=AXIS2_PLACEMENT_3D ( 'NONE', #13624, #2074, #771 ) ;
#5583=ORIENTED_EDGE ( 'NONE', *, *, #1860, .T. ) ;
#5586=VERTEX_POINT ( 'NONE', #11204 ) ;
#5594=DIRECTION ( 'NONE',  ( 1.000000000000000000, 1.000000000000000078E-15, 0.000000000000000000 ) ) ;
#5670=DIRECTION ( 'NONE',  ( -8.673617379884027583E-16, 1.000000000000000000, 0.000000000000000000 ) ) ;
#5676=ORIENTED_EDGE ( 'NONE', *, *, #7323, .F. ) ;
#5735=UNCERTAINTY_MEASURE_WITH_UNIT (LENGTH_MEASURE( 1.000000000000000082E-05 ), #10106, 'distance_accuracy_value', 'NONE');
#5768=VERTEX_POINT ( 'NONE', #7277 ) ;
#5828=VERTEX_POINT ( 'NONE', #9810 ) ;
#5839=VERTEX_POINT ( 'NONE', #14479 ) ;
#5853=CARTESIAN_POINT ( 'NONE',  ( -9.508527451665001351, -44.50737899243799944, -5.497689735156000346 ) ) ;
#5879=ORIENTED_EDGE ( 'NONE', *, *, #3883, .T. ) ;
#5911=VECTOR ( 'NONE', #2217, 1000.000000000000000 ) ;
#5926=EDGE_CURVE ( 'NONE', #5586, #12315, #8806, .T. ) ;
#5964=ADVANCED_FACE ( 'NONE', ( #6354 ), #11029, .T. ) ;
#6052=ORIENTED_EDGE ( 'NONE', *, *, #266, .F. ) ;
#6060=ADVANCED_FACE ( 'NONE', ( #2082 ), #11407, .F. ) ;
#6067=DIRECTION ( 'NONE',  ( 1.000000000000000000, 1.000000000000000078E-15, 0.000000000000000000 ) ) ;
#6091=ORIENTED_EDGE ( 'NONE', *, *, #1314, .T. ) ;
#6096=( GEOMETRIC_REPRESENTATION_CONTEXT ( 3 ) GLOBAL_UNCERTAINTY_ASSIGNED_CONTEXT ( ( #4326 ) ) GLOBAL_UNIT_ASSIGNED_CONTEXT ( ( #4858, #10662, #12045 ) ) REPRESENTATION_CONTEXT ( 'NONE', 'WORKASPACE' ) );
#6125=ORIENTED_EDGE ( 'NONE', *, *, #3838, .F. ) ;
#6148=VECTOR ( 'NONE', #12185, 1000.000000000000000 ) ;
#6254=EDGE_CURVE ( 'NONE', #415, #2422, #6920, .T. ) ;
#6263=VECTOR ( 'NONE', #2689, 999.9999999999998863 ) ;
#6269=SHAPE_DEFINITION_REPRESENTATION ( #793, #3931 ) ;
#6322=AXIS2_PLACEMENT_3D ( 'NONE', #627, #8654, #9949 ) ;
#6354=FACE_OUTER_BOUND ( 'NONE', #11425, .T. ) ;
#6408=ORIENTED_EDGE ( 'NONE', *, *, #14044, .F. ) ;
#6459=EDGE_CURVE ( 'NONE', #1750, #14475, #6596, .T. ) ;
#6476=VERTEX_POINT ( 'NONE', #8977 ) ;
#6498=ORIENTED_EDGE ( 'NONE', *, *, #9633, .F. ) ;
#6520=AXIS2_PLACEMENT_3D ( 'NONE', #2999, #8881, #4227 ) ;
#6522=DIRECTION ( 'NONE',  ( 1.000000000000000000, 1.000000000000000078E-15, 0.000000000000000000 ) ) ;
#6525=CARTESIAN_POINT ( 'NONE',  ( -9.989347722329672052, -48.50737899243800655, -5.497689735156000346 ) ) ;
#6578=CARTESIAN_POINT ( 'NONE',  ( -3.508527451665001351, -44.77532818486911736, -5.497689735156003010 ) ) ;
#6596=LINE ( 'NONE', #6525, #7997 ) ;
#6634=VECTOR ( 'NONE', #10830, 1000.000000000000000 ) ;
#6672=DIRECTION ( 'NONE',  ( 1.000000000000000000, 1.000000000000000078E-15, 0.000000000000000000 ) ) ;
#6683=CARTESIAN_POINT ( 'NONE',  ( -3.508527451664998686, -47.80641709811465745, -4.747689735156000346 ) ) ;
#6731=ADVANCED_FACE ( 'NONE', ( #8648 ), #1616, .T. ) ;
#6764=PRODUCT ( 'Slide Locking Screw', 'Slide Locking Screw', '', ( #3835 ) ) ;
#6789=AXIS2_PLACEMENT_3D ( 'NONE', #4381, #12419, #6809 ) ;
#6809=DIRECTION ( 'NONE',  ( 1.000000000000000000, 0.000000000000000000, 0.000000000000000000 ) ) ;
#6838=ORIENTED_EDGE ( 'NONE', *, *, #14300, .T. ) ;
#6857=ORIENTED_EDGE ( 'NONE', *, *, #7323, .T. ) ;
#6862=CARTESIAN_POINT ( 'NONE',  ( -1.508527451664997798, -48.23942980000687442, -5.497689735155999458 ) ) ;
#6878=VECTOR ( 'NONE', #8318, 1000.000000000000000 ) ;
#6920=LINE ( 'NONE', #8230, #7986 ) ;
#6938=VECTOR ( 'NONE', #1, 1000.000000000000000 ) ;
#6960=CARTESIAN_POINT ( 'NONE',  ( -1.508527451664999575, -45.64135358865355130, -6.997689735156000346 ) ) ;
#6961=ORIENTED_EDGE ( 'NONE', *, *, #12248, .F. ) ;
#7021=FACE_OUTER_BOUND ( 'NONE', #7119, .T. ) ;
#7041=EDGE_LOOP ( 'NONE', ( #574, #9657, #2228, #8641 ) ) ;
#7050=PRODUCT_DEFINITION_FORMATION_WITH_SPECIFIED_SOURCE ( 'ANY', '', #6764, .NOT_KNOWN. ) ;
#7075=ORIENTED_EDGE ( 'NONE', *, *, #3838, .T. ) ;
#7119=EDGE_LOOP ( 'NONE', ( #1111, #12334, #14606, #10133 ) ) ;
#7154=CIRCLE ( 'NONE', #7647, 2.458500000000002572 ) ;
#7169=CARTESIAN_POINT ( 'NONE',  ( -3.508527451664997798, -48.23942980000687442, -5.497689735155999458 ) ) ;
#7199=ORIENTED_EDGE ( 'NONE', *, *, #1524, .F. ) ;
#7238=CARTESIAN_POINT ( 'NONE',  ( -7.758527451664999575, -46.50737899243799944, -5.497689735156000346 ) ) ;
#7251=CIRCLE ( 'NONE', #11175, 3.000000000000002665 ) ;
#7275=LINE ( 'NONE', #114, #1761 ) ;
#7277=CARTESIAN_POINT ( 'NONE',  ( -1.508527451664997354, -48.96587899243800024, -5.497689735156000346 ) ) ;
#7294=EDGE_CURVE ( 'NONE', #12315, #7352, #10625, .T. ) ;
#7299=CARTESIAN_POINT ( 'NONE',  ( -1.508527451664997798, -47.80641709811465034, -4.747689735156000346 ) ) ;
#7306=VECTOR ( 'NONE', #3038, 1000.000000000000000 ) ;
#7310=DIRECTION ( 'NONE',  ( -1.011922027653136551E-15, 1.000000000000000000, 0.000000000000000000 ) ) ;
#7316=ORIENTED_EDGE ( 'NONE', *, *, #7294, .F. ) ;
#7323=EDGE_CURVE ( 'NONE', #5828, #2471, #4741, .T. ) ;
#7352=VERTEX_POINT ( 'NONE', #6862 ) ;
#7387=CARTESIAN_POINT ( 'NONE',  ( -9.508527451664999575, -46.50737899243799944, -5.497689735156000346 ) ) ;
#7399=ADVANCED_FACE ( 'NONE', ( #5463 ), #4761, .T. ) ;
#7406=EDGE_LOOP ( 'NONE', ( #2462, #3974 ) ) ;
#7495=PRODUCT_DEFINITION ( 'UNKNOWN', '', #7050, #4673 ) ;
#7498=DIRECTION ( 'NONE',  ( -1.000000000000000000, -1.000000000000000078E-15, 0.000000000000000000 ) ) ;
#7566=MANIFOLD_SOLID_BREP ( 'Stock-MAS-672-1', #4877 ) ;
#7583=ORIENTED_EDGE ( 'NONE', *, *, #5415, .F. ) ;
#7605=DIRECTION ( 'NONE',  ( -8.673617379884027583E-16, 1.000000000000000000, 0.000000000000000000 ) ) ;
#7629=ORIENTED_EDGE ( 'NONE', *, *, #3003, .F. ) ;
#7642=LINE ( 'NONE', #3138, #13142 ) ;
#7647=AXIS2_PLACEMENT_3D ( 'NONE', #9980, #3178, #4176 ) ;
#7698=ORIENTED_EDGE ( 'NONE', *, *, #2120, .T. ) ;
#7785=EDGE_CURVE ( 'NONE', #13801, #2422, #786, .T. ) ;
#7830=DIRECTION ( 'NONE',  ( 1.011922027653136551E-15, -1.000000000000000000, 0.000000000000000000 ) ) ;
#7854=ADVANCED_FACE ( 'NONE', ( #13792 ), #2166, .T. ) ;
#7859=VECTOR ( 'NONE', #12698, 1000.000000000000000 ) ;
#7958=CARTESIAN_POINT ( 'NONE',  ( -9.989347722329673829, -46.50737899243799944, -5.497689735156000346 ) ) ;
#7965=ORIENTED_EDGE ( 'NONE', *, *, #5145, .T. ) ;
#7986=VECTOR ( 'NONE', #3650, 1000.000000000000000 ) ;
#7992=CARTESIAN_POINT ( 'NONE',  ( -3.508527451664998686, -47.37340439622244048, -3.997689735156000790 ) ) ;
#7997=VECTOR ( 'NONE', #10049, 1000.000000000000000 ) ;
#8032=EDGE_LOOP ( 'NONE', ( #6125, #6091, #5583, #4332 ) ) ;
#8108=DIRECTION ( 'NONE',  ( 1.000000000000000000, 1.000000000000000078E-15, 0.000000000000000000 ) ) ;
#8113=CONICAL_SURFACE ( 'NONE', #2762, 2.000000000000001776, 0.7853981633974476129 ) ;
#8119=EDGE_CURVE ( 'NONE', #14475, #11680, #9798, .T. ) ;
#8193=DIRECTION ( 'NONE',  ( 1.000000000000000078E-15, -1.000000000000000000, 0.000000000000000000 ) ) ;
#8230=CARTESIAN_POINT ( 'NONE',  ( -1.508527451665001351, -45.20834088676132723, -4.747689735156000346 ) ) ;
#8273=ORIENTED_EDGE ( 'NONE', *, *, #5415, .T. ) ;
#8297=DIRECTION ( 'NONE',  ( 1.000000000000000000, 1.000000000000000078E-15, 0.000000000000000000 ) ) ;
#8315=EDGE_LOOP ( 'NONE', ( #8273, #5879, #4554, #2687, #14422, #1768 ) ) ;
#8318=DIRECTION ( 'NONE',  ( -1.000000000000000078E-15, 1.000000000000000000, 0.000000000000000000 ) ) ;
#8341=FACE_OUTER_BOUND ( 'NONE', #2441, .T. ) ;
#8386=AXIS2_PLACEMENT_3D ( 'NONE', #6683, #11367, #890 ) ;
#8455=EDGE_CURVE ( 'NONE', #3528, #7352, #13314, .T. ) ;
#8463=CARTESIAN_POINT ( 'NONE',  ( -1.821162622431179878, -46.50737899243799234, -5.497689735156000346 ) ) ;
#8475=DIRECTION ( 'NONE',  ( 1.000000000000000000, 1.000000000000000078E-15, 0.000000000000000000 ) ) ;
#8516=( GEOMETRIC_REPRESENTATION_CONTEXT ( 3 ) GLOBAL_UNCERTAINTY_ASSIGNED_CONTEXT ( ( #5735 ) ) GLOBAL_UNIT_ASSIGNED_CONTEXT ( ( #10106, #2089, #10416 ) ) REPRESENTATION_CONTEXT ( 'NONE', 'WORKASPACE' ) );
#8523=EDGE_LOOP ( 'NONE', ( #7629, #10215, #12597, #13582, #10349, #9805 ) ) ;
#8535=AXIS2_PLACEMENT_3D ( 'NONE', #14857, #13710, #3231 ) ;
#8539=CARTESIAN_POINT ( 'NONE',  ( -3.508527451664999575, -46.50737899243799234, -3.997689735156000790 ) ) ;
#8641=ORIENTED_EDGE ( 'NONE', *, *, #10445, .F. ) ;
#8648=FACE_OUTER_BOUND ( 'NONE', #7041, .T. ) ;
#8654=DIRECTION ( 'NONE',  ( -1.000000000000000000, -1.000000000000000078E-15, -0.000000000000000000 ) ) ;
#8658=CARTESIAN_POINT ( 'NONE',  ( -3.508527451664998686, -47.80641709811465745, -6.247689735156000346 ) ) ;
#8722=EDGE_CURVE ( 'NONE', #1750, #13341, #12651, .T. ) ;
#8764=ADVANCED_FACE ( 'NONE', ( #12235 ), #1673, .T. ) ;
#8776=EDGE_CURVE ( 'NONE', #14925, #8983, #7251, .T. ) ;
#8806=LINE ( 'NONE', #8658, #6148 ) ;
#8881=DIRECTION ( 'NONE',  ( 0.000000000000000000, 0.000000000000000000, 1.000000000000000000 ) ) ;
#8929=DIRECTION ( 'NONE',  ( 1.000000000000000000, 1.000000000000000078E-15, 0.000000000000000000 ) ) ;
#8954=EDGE_LOOP ( 'NONE', ( #605, #6408, #13989, #10191 ) ) ;
#8977=CARTESIAN_POINT ( 'NONE',  ( -6.758527451665002239, -43.50737899243799944, -5.497689735156000346 ) ) ;
#8983=VERTEX_POINT ( 'NONE', #13072 ) ;
#8990=EDGE_CURVE ( 'NONE', #8983, #14925, #13864, .T. ) ;
#9034=EDGE_CURVE ( 'NONE', #13341, #1750, #14105, .T. ) ;
#9058=CARTESIAN_POINT ( 'NONE',  ( -1.508527451664999575, -45.64135358865355130, -3.997689735156000790 ) ) ;
#9082=CONICAL_SURFACE ( 'NONE', #2492, 3.000000000000002665, 1.047197551196598297 ) ;
#9109=DIRECTION ( 'NONE',  ( 1.000000000000000000, 1.000000000000000078E-15, 0.000000000000000000 ) ) ;
#9208=AXIS2_PLACEMENT_3D ( 'NONE', #7387, #2433, #11753 ) ;
#9219=VECTOR ( 'NONE', #9392, 1000.000000000000000 ) ;
#9360=ORIENTED_EDGE ( 'NONE', *, *, #2120, .F. ) ;
#9367=AXIS2_PLACEMENT_3D ( 'NONE', #8539, #11833, #2498 ) ;
#9392=DIRECTION ( 'NONE',  ( -5.000000000000000389E-16, 0.4999999999999998890, -0.8660254037844387076 ) ) ;
#9432=DIRECTION ( 'NONE',  ( 1.000000000000000000, 1.000000000000000078E-15, 0.000000000000000000 ) ) ;
#9633=EDGE_CURVE ( 'NONE', #2471, #3528, #12731, .T. ) ;
#9657=ORIENTED_EDGE ( 'NONE', *, *, #6459, .T. ) ;
#9689=ORIENTED_EDGE ( 'NONE', *, *, #8776, .T. ) ;
#9720=CARTESIAN_POINT ( 'NONE',  ( -1.508527451664999575, -47.37340439622244048, -6.997689735156000346 ) ) ;
#9730=AXIS2_PLACEMENT_3D ( 'NONE', #11173, #1689, #13334 ) ;
#9746=VECTOR ( 'NONE', #4075, 1000.000000000000000 ) ;
#9752=ORIENTED_EDGE ( 'NONE', *, *, #590, .T. ) ;
#9798=LINE ( 'NONE', #12170, #6263 ) ;
#9805=ORIENTED_EDGE ( 'NONE', *, *, #2763, .F. ) ;
#9810=CARTESIAN_POINT ( 'NONE',  ( -3.508527451665000463, -45.64135358865355840, -6.997689735156000346 ) ) ;
#9878=VECTOR ( 'NONE', #8193, 1000.000000000000000 ) ;
#9920=CARTESIAN_POINT ( 'NONE',  ( -3.508527451665000463, -45.20834088676133433, -6.247689735156000346 ) ) ;
#9945=AXIS2_PLACEMENT_3D ( 'NONE', #13562, #9109, #3070 ) ;
#9949=DIRECTION ( 'NONE',  ( 0.000000000000000000, 0.000000000000000000, -1.000000000000000000 ) ) ;
#9960=CARTESIAN_POINT ( 'NONE',  ( -1.508527451665001351, -45.20834088676132723, -6.247689735156000346 ) ) ;
#9980=CARTESIAN_POINT ( 'NONE',  ( -1.508527451664999575, -46.50737899243799234, -5.497689735156000346 ) ) ;
#10005=ADVANCED_FACE ( 'NONE', ( #7021 ), #4907, .T. ) ;
#10049=DIRECTION ( 'NONE',  ( 1.000000000000000000, 1.000000000000000078E-15, 0.000000000000000000 ) ) ;
#10106=( LENGTH_UNIT ( ) NAMED_UNIT ( * ) SI_UNIT ( .MILLI., .METRE. ) );
#10133=ORIENTED_EDGE ( 'NONE', *, *, #7294, .T. ) ;
#10179=CYLINDRICAL_SURFACE ( 'NONE', #8535, 3.000000000000002665 ) ;
#10190=CARTESIAN_POINT ( 'NONE',  ( -1.508527451664999575, -46.50737899243799234, -6.997689735156000346 ) ) ;
#10191=ORIENTED_EDGE ( 'NONE', *, *, #7785, .T. ) ;
#10199=VECTOR ( 'NONE', #10934, 999.9999999999998863 ) ;
#10215=ORIENTED_EDGE ( 'NONE', *, *, #5926, .F. ) ;
#10224=LINE ( 'NONE', #7992, #2190 ) ;
#10259=VECTOR ( 'NONE', #5594, 1000.000000000000000 ) ;
#10265=AXIS2_PLACEMENT_3D ( 'NONE', #7958, #1012, #5670 ) ;
#10269=ADVANCED_FACE ( 'NONE', ( #11442 ), #9082, .T. ) ;
#10308=CARTESIAN_POINT ( 'NONE',  ( -9.508527451664997798, -48.50737899243800655, -5.497689735156000346 ) ) ;
#10340=CIRCLE ( 'NONE', #3758, 2.458500000000002572 ) ;
#10349=ORIENTED_EDGE ( 'NONE', *, *, #1650, .F. ) ;
#10384=ORIENTED_EDGE ( 'NONE', *, *, #8776, .F. ) ;
#10416=( NAMED_UNIT ( * ) SI_UNIT ( $, .STERADIAN. ) SOLID_ANGLE_UNIT ( ) );
#10433=CONICAL_SURFACE ( 'NONE', #14838, 3.000000000000002665, 1.047197551196598297 ) ;
#10445=EDGE_CURVE ( 'NONE', #13341, #11896, #7275, .T. ) ;
#10471=LINE ( 'NONE', #2214, #6878 ) ;
#10563=EDGE_LOOP ( 'NONE', ( #311, #12224 ) ) ;
#10586=AXIS2_PLACEMENT_3D ( 'NONE', #3789, #6067, #10749 ) ;
#10613=FACE_OUTER_BOUND ( 'NONE', #8954, .T. ) ;
#10625=LINE ( 'NONE', #7169, #6938 ) ;
#10662=( NAMED_UNIT ( * ) PLANE_ANGLE_UNIT ( ) SI_UNIT ( $, .RADIAN. ) );
#10675=VECTOR ( 'NONE', #13457, 1000.000000000000000 ) ;
#10749=DIRECTION ( 'NONE',  ( -8.673617379884027583E-16, 1.000000000000000000, 0.000000000000000000 ) ) ;
#10760=MECHANICAL_DESIGN_GEOMETRIC_PRESENTATION_REPRESENTATION('',(#741),#6096);
#10766=FACE_OUTER_BOUND ( 'NONE', #13539, .T. ) ;
#10818=FILL_AREA_STYLE_COLOUR ( '', #1474 ) ;
#10830=DIRECTION ( 'NONE',  ( -5.000000000000000389E-16, 0.4999999999999998890, 0.8660254037844387076 ) ) ;
#10934=DIRECTION ( 'NONE',  ( 0.7071067811865473507, 0.7071067811865477948, 0.000000000000000000 ) ) ;
#10960=FACE_BOUND ( 'NONE', #8315, .T. ) ;
#11029=PLANE ( 'NONE',  #6520 ) ;
#11041=CIRCLE ( 'NONE', #1526, 2.000000000000001776 ) ;
#11152=LINE ( 'NONE', #9920, #7306 ) ;
#11173=CARTESIAN_POINT ( 'NONE',  ( -9.989347722329673829, -46.50737899243799944, -5.497689735156000346 ) ) ;
#11175=AXIS2_PLACEMENT_3D ( 'NONE', #13463, #756, #606 ) ;
#11204=CARTESIAN_POINT ( 'NONE',  ( -3.508527451664998686, -47.37340439622244048, -6.997689735156000346 ) ) ;
#11217=ORIENTED_EDGE ( 'NONE', *, *, #14390, .T. ) ;
#11223=DIRECTION ( 'NONE',  ( 1.000000000000000000, 1.000000000000000078E-15, 0.000000000000000000 ) ) ;
#11313=ORIENTED_EDGE ( 'NONE', *, *, #7785, .F. ) ;
#11341=VECTOR ( 'NONE', #8297, 1000.000000000000000 ) ;
#11353=AXIS2_PLACEMENT_3D ( 'NONE', #5245, #6522, #7605 ) ;
#11367=DIRECTION ( 'NONE',  ( -8.660254037844387408E-16, 0.8660254037844387076, -0.4999999999999998890 ) ) ;
#11407=PLANE ( 'NONE',  #9945 ) ;
#11425=EDGE_LOOP ( 'NONE', ( #6498, #5676, #3922, #4336 ) ) ;
#11442=FACE_OUTER_BOUND ( 'NONE', #4604, .T. ) ;
#11546=CARTESIAN_POINT ( 'NONE',  ( -3.508527451665000463, -45.64135358865355840, -6.997689735156000346 ) ) ;
#11635=CARTESIAN_POINT ( 'NONE',  ( -9.989347722329673829, -46.50737899243799944, -5.497689735156000346 ) ) ;
#11652=EDGE_LOOP ( 'NONE', ( #6052, #6961, #9752, #3735 ) ) ;
#11680=VERTEX_POINT ( 'NONE', #12791 ) ;
#11699=DIRECTION ( 'NONE',  ( 1.000000000000000000, 1.000000000000000078E-15, 0.000000000000000000 ) ) ;
#11748=ADVANCED_FACE ( 'NONE', ( #10 ), #4905, .T. ) ;
#11753=DIRECTION ( 'NONE',  ( -8.673617379884027583E-16, 1.000000000000000000, 0.000000000000000000 ) ) ;
#11754=DIRECTION ( 'NONE',  ( 4.999999999999998416E-16, -0.4999999999999998890, 0.8660254037844387076 ) ) ;
#11779=DIRECTION ( 'NONE',  ( -1.000000000000000000, -1.000000000000000078E-15, 0.000000000000000000 ) ) ;
#11809=PRESENTATION_STYLE_ASSIGNMENT (( #3852 ) ) ;
#11816=ORIENTED_EDGE ( 'NONE', *, *, #2763, .T. ) ;
#11833=DIRECTION ( 'NONE',  ( -0.000000000000000000, 0.000000000000000000, -1.000000000000000000 ) ) ;
#11875=EDGE_LOOP ( 'NONE', ( #2240, #7698, #912, #12076 ) ) ;
#11896=VERTEX_POINT ( 'NONE', #4147 ) ;
#11912=EDGE_LOOP ( 'NONE', ( #7583, #7316, #1923, #11217 ) ) ;
#11914=DIRECTION ( 'NONE',  ( 1.000000000000000000, 1.000000000000000078E-15, 0.000000000000000000 ) ) ;
#11932=LINE ( 'NONE', #2673, #3078 ) ;
#11973=CARTESIAN_POINT ( 'NONE',  ( -3.508527451664998686, -47.37340439622244048, -3.997689735156000790 ) ) ;
#12045=( NAMED_UNIT ( * ) SI_UNIT ( $, .STERADIAN. ) SOLID_ANGLE_UNIT ( ) );
#12076=ORIENTED_EDGE ( 'NONE', *, *, #1314, .F. ) ;
#12170=CARTESIAN_POINT ( 'NONE',  ( -7.758527451664997798, -48.50737899243800655, -5.497689735156000346 ) ) ;
#12185=DIRECTION ( 'NONE',  ( 5.000000000000000389E-16, -0.4999999999999998890, 0.8660254037844387076 ) ) ;
#12195=LINE ( 'NONE', #1710, #15005 ) ;
#12224=ORIENTED_EDGE ( 'NONE', *, *, #8722, .F. ) ;
#12235=FACE_OUTER_BOUND ( 'NONE', #8523, .T. ) ;
#12236=CARTESIAN_POINT ( 'NONE',  ( -7.758527451665001351, -44.50737899243799944, -5.497689735156000346 ) ) ;
#12248=EDGE_CURVE ( 'NONE', #5768, #5839, #10340, .T. ) ;
#12257=FACE_OUTER_BOUND ( 'NONE', #7406, .T. ) ;
#12304=CARTESIAN_POINT ( 'NONE',  ( -1.508527451664997798, -47.80641709811465034, -6.247689735156000346 ) ) ;
#12315=VERTEX_POINT ( 'NONE', #2289 ) ;
#12334=ORIENTED_EDGE ( 'NONE', *, *, #12759, .F. ) ;
#12416=VECTOR ( 'NONE', #14066, 999.9999999999998863 ) ;
#12419=DIRECTION ( 'NONE',  ( 0.000000000000000000, 0.000000000000000000, 1.000000000000000000 ) ) ;
#12514=FACE_OUTER_BOUND ( 'NONE', #11912, .T. ) ;
#12597=ORIENTED_EDGE ( 'NONE', *, *, #13048, .F. ) ;
#12651=CIRCLE ( 'NONE', #1406, 2.000000000000001776 ) ;
#12683=DIRECTION ( 'NONE',  ( 1.000000000000000000, 1.000000000000000078E-15, 0.000000000000000000 ) ) ;
#12691=PLANE ( 'NONE',  #13380 ) ;
#12698=DIRECTION ( 'NONE',  ( 1.000000000000000000, 1.000000000000000078E-15, 0.000000000000000000 ) ) ;
#12703=CARTESIAN_POINT ( 'NONE',  ( -3.508527451665000463, -45.64135358865355840, -3.997689735156000790 ) ) ;
#12711=EDGE_LOOP ( 'NONE', ( #13740, #1078, #13703, #9360 ) ) ;
#12731=LINE ( 'NONE', #10190, #3860 ) ;
#12759=EDGE_CURVE ( 'NONE', #5586, #3528, #824, .T. ) ;
#12791=CARTESIAN_POINT ( 'NONE',  ( -6.758527451664997798, -49.50737899243800655, -5.497689735156000346 ) ) ;
#12938=LINE ( 'NONE', #12703, #5911 ) ;
#12948=AXIS2_PLACEMENT_3D ( 'NONE', #11635, #8108, #1154 ) ;
#12968=ORIENTED_EDGE ( 'NONE', *, *, #13552, .F. ) ;
#12972=SURFACE_STYLE_FILL_AREA ( #350 ) ;
#13021=DIRECTION ( 'NONE',  ( 8.660254037844387408E-16, -0.8660254037844387076, 0.4999999999999998890 ) ) ;
#13026=ORIENTED_EDGE ( 'NONE', *, *, #5145, .F. ) ;
#13048=EDGE_CURVE ( 'NONE', #5828, #5586, #4690, .T. ) ;
#13072=CARTESIAN_POINT ( 'NONE',  ( -1.821162622431176770, -49.50737899243799944, -5.497689735156000346 ) ) ;
#13138=LINE ( 'NONE', #7299, #6634 ) ;
#13142=VECTOR ( 'NONE', #622, 1000.000000000000000 ) ;
#13151=CARTESIAN_POINT ( 'NONE',  ( -9.989347722329677381, -43.50737899243799944, -5.497689735156000346 ) ) ;
#13228=CARTESIAN_POINT ( 'NONE',  ( -6.758527451664999575, -46.50737899243799944, -5.497689735156000346 ) ) ;
#13290=CIRCLE ( 'NONE', #10586, 2.000000000000001776 ) ;
#13314=LINE ( 'NONE', #12304, #10675 ) ;
#13334=DIRECTION ( 'NONE',  ( -8.673617379884027583E-16, 1.000000000000000000, 0.000000000000000000 ) ) ;
#13335=CARTESIAN_POINT ( 'NONE',  ( -1.821162622431179878, -46.50737899243799234, -5.497689735156000346 ) ) ;
#13341=VERTEX_POINT ( 'NONE', #5853 ) ;
#13380=AXIS2_PLACEMENT_3D ( 'NONE', #3349, #145, #11754 ) ;
#13404=ADVANCED_FACE ( 'NONE', ( #10766 ), #290, .T. ) ;
#13457=DIRECTION ( 'NONE',  ( 5.000000000000000389E-16, -0.4999999999999998890, 0.8660254037844387076 ) ) ;
#13463=CARTESIAN_POINT ( 'NONE',  ( -1.821162622431179878, -46.50737899243799234, -5.497689735156000346 ) ) ;
#13471=CARTESIAN_POINT ( 'NONE',  ( -3.508527451665001351, -44.77532818486911736, -5.497689735156003010 ) ) ;
#13534=CARTESIAN_POINT ( 'NONE',  ( -9.508527451664999575, -46.50737899243799944, -5.497689735156000346 ) ) ;
#13539=EDGE_LOOP ( 'NONE', ( #5252, #1659, #11816, #1284 ) ) ;
#13552=EDGE_CURVE ( 'NONE', #5839, #5768, #7154, .T. ) ;
#13562=CARTESIAN_POINT ( 'NONE',  ( -9.508527451665001351, -45.50737899243799944, -5.497689735156000346 ) ) ;
#13582=ORIENTED_EDGE ( 'NONE', *, *, #14300, .F. ) ;
#13624=CARTESIAN_POINT ( 'NONE',  ( -6.758527451664999575, -46.50737899243799944, -5.497689735156000346 ) ) ;
#13672=CARTESIAN_POINT ( 'NONE',  ( -1.821162622431179878, -46.50737899243799234, -5.497689735156000346 ) ) ;
#13688=DIRECTION ( 'NONE',  ( 1.000000000000000000, 1.000000000000000078E-15, 0.000000000000000000 ) ) ;
#13703=ORIENTED_EDGE ( 'NONE', *, *, #10445, .T. ) ;
#13710=DIRECTION ( 'NONE',  ( 1.000000000000000000, 1.000000000000000078E-15, 0.000000000000000000 ) ) ;
#13740=ORIENTED_EDGE ( 'NONE', *, *, #6459, .F. ) ;
#13792=FACE_OUTER_BOUND ( 'NONE', #12711, .T. ) ;
#13801=VERTEX_POINT ( 'NONE', #13471 ) ;
#13864=CIRCLE ( 'NONE', #670, 3.000000000000002665 ) ;
#13878=FACE_OUTER_BOUND ( 'NONE', #11875, .T. ) ;
#13989=ORIENTED_EDGE ( 'NONE', *, *, #1650, .T. ) ;
#13992=LINE ( 'NONE', #3664, #7859 ) ;
#14044=EDGE_CURVE ( 'NONE', #374, #415, #12938, .T. ) ;
#14066=DIRECTION ( 'NONE',  ( -0.5000000000000004441, 0.8660254037844384856, 1.060575238724907408E-16 ) ) ;
#14105=CIRCLE ( 'NONE', #9208, 2.000000000000001776 ) ;
#14180=EDGE_CURVE ( 'NONE', #11896, #14475, #11041, .T. ) ;
#14218=AXIS2_PLACEMENT_3D ( 'NONE', #86, #4600, #11779 ) ;
#14300=EDGE_CURVE ( 'NONE', #13801, #5828, #11152, .T. ) ;
#14383=LINE ( 'NONE', #12236, #10199 ) ;
#14390=EDGE_CURVE ( 'NONE', #1143, #4490, #10224, .T. ) ;
#14422=ORIENTED_EDGE ( 'NONE', *, *, #9633, .T. ) ;
#14475=VERTEX_POINT ( 'NONE', #2276 ) ;
#14479=CARTESIAN_POINT ( 'NONE',  ( -1.508527451665002017, -44.04887899243799154, -5.497689735156000346 ) ) ;
#14606=ORIENTED_EDGE ( 'NONE', *, *, #5926, .T. ) ;
#14786=SHAPE_REPRESENTATION_RELATIONSHIP ( 'NONE' , 'NONE' ,  #3931, #3153 ) ;
#14838=AXIS2_PLACEMENT_3D ( 'NONE', #13335, #7498, #1618 ) ;
#14857=CARTESIAN_POINT ( 'NONE',  ( -9.989347722329673829, -46.50737899243799944, -5.497689735156000346 ) ) ;
#14869=VECTOR ( 'NONE', #11914, 1000.000000000000000 ) ;
#14925=VERTEX_POINT ( 'NONE', #121 ) ;
#14944=ORIENTED_EDGE ( 'NONE', *, *, #590, .F. ) ;
#15005=VECTOR ( 'NONE', #4161, 1000.000000000000114 ) ;
#15117=EDGE_CURVE ( 'NONE', #2422, #2471, #3930, .T. ) ;
ENDSEC;
END-ISO-10303-21;
